ISO-10303-21;
HEADER;
/* Generated by software containing ST-Developer
 * from STEP Tools, Inc. (www.steptools.com) 
 */

FILE_DESCRIPTION(
/* description */ ('Rigid flange shaft coupling assembly'),
/* implementation_level */ '2;1');

FILE_NAME(
/* name */ 'Cap Screw - M5x20.step',
/* time_stamp */ '2026-10-27T10:47:16-07:00',
/* author */ (''),
/* organization */ (''),
/* preprocessor_version */ 'ST-DEVELOPER v20.2',
/* originating_system */ 'Autodesk Translation Framework v15.17.0.0',
/* authorisation */ '');

FILE_SCHEMA (('AUTOMOTIVE_DESIGN { 1 0 10303 214 3 1 1 }'));
ENDSEC;

DATA;
#10=MECHANICAL_DESIGN_GEOMETRIC_PRESENTATION_REPRESENTATION('',(#422),#9141);
#26=CONICAL_SURFACE('',#5489,0.4,0.785398163397448);
#27=CONICAL_SURFACE('',#5493,0.41,0.785398163397448);
#28=CONICAL_SURFACE('',#5497,0.26,0.463647609000806);
#29=CONICAL_SURFACE('',#5501,0.225,0.785398163397448);
#39=ORIENTED_CLOSED_SHELL('',*,#4778,.F.);
#42=BREP_WITH_VOIDS('Body1',#4777,(#39));
#365=SHAPE_REPRESENTATION_RELATIONSHIP('SRR','None',#9301,#393);
#393=ADVANCED_BREP_SHAPE_REPRESENTATION('',(#42),#9136);
#422=STYLED_ITEM('',(#9507),#42);
#563=FACE_BOUND('',#1342,.T.);
#703=PLANE('',#5487);
#704=PLANE('',#5495);
#705=PLANE('',#5503);
#706=PLANE('',#5504);
#707=PLANE('',#5505);
#708=PLANE('',#5506);
#709=PLANE('',#5507);
#710=PLANE('',#5508);
#711=PLANE('',#5509);
#712=PLANE('',#5510);
#713=PLANE('',#5511);
#955=FACE_OUTER_BOUND('',#1337,.T.);
#956=FACE_OUTER_BOUND('',#1338,.T.);
#957=FACE_OUTER_BOUND('',#1339,.T.);
#958=FACE_OUTER_BOUND('',#1340,.T.);
#959=FACE_OUTER_BOUND('',#1341,.T.);
#960=FACE_OUTER_BOUND('',#1343,.T.);
#961=FACE_OUTER_BOUND('',#1344,.T.);
#962=FACE_OUTER_BOUND('',#1345,.T.);
#963=FACE_OUTER_BOUND('',#1346,.T.);
#964=FACE_OUTER_BOUND('',#1347,.T.);
#965=FACE_OUTER_BOUND('',#1348,.T.);
#966=FACE_OUTER_BOUND('',#1349,.T.);
#967=FACE_OUTER_BOUND('',#1350,.T.);
#968=FACE_OUTER_BOUND('',#1351,.T.);
#969=FACE_OUTER_BOUND('',#1352,.T.);
#970=FACE_OUTER_BOUND('',#1353,.T.);
#971=FACE_OUTER_BOUND('',#1354,.T.);
#1337=EDGE_LOOP('',(#4159));
#1338=EDGE_LOOP('',(#4160,#4161,#4162,#4163));
#1339=EDGE_LOOP('',(#4164,#4165,#4166,#4167));
#1340=EDGE_LOOP('',(#4168,#4169,#4170,#4171));
#1341=EDGE_LOOP('',(#4172));
#1342=EDGE_LOOP('',(#4173));
#1343=EDGE_LOOP('',(#4174,#4175,#4176,#4177));
#1344=EDGE_LOOP('',(#4178,#4179,#4180,#4181));
#1345=EDGE_LOOP('',(#4182,#4183,#4184,#4185));
#1346=EDGE_LOOP('',(#4186));
#1347=EDGE_LOOP('',(#4187,#4188,#4189,#4190));
#1348=EDGE_LOOP('',(#4191,#4192,#4193,#4194));
#1349=EDGE_LOOP('',(#4195,#4196,#4197,#4198));
#1350=EDGE_LOOP('',(#4199,#4200,#4201,#4202));
#1351=EDGE_LOOP('',(#4203,#4204,#4205,#4206));
#1352=EDGE_LOOP('',(#4207,#4208,#4209,#4210));
#1353=EDGE_LOOP('',(#4211,#4212,#4213,#4214,#4215,#4216));
#1354=EDGE_LOOP('',(#4217,#4218,#4219,#4220,#4221,#4222));
#1670=LINE('',#8735,#2015);
#1671=LINE('',#8739,#2016);
#1672=LINE('',#8743,#2017);
#1673=LINE('',#8750,#2018);
#1674=LINE('',#8754,#2019);
#1675=LINE('',#8758,#2020);
#1676=LINE('',#8763,#2021);
#1677=LINE('',#8765,#2022);
#1678=LINE('',#8767,#2023);
#1679=LINE('',#8768,#2024);
#1680=LINE('',#8771,#2025);
#1681=LINE('',#8773,#2026);
#1682=LINE('',#8774,#2027);
#1683=LINE('',#8777,#2028);
#1684=LINE('',#8779,#2029);
#1685=LINE('',#8780,#2030);
#1686=LINE('',#8783,#2031);
#1687=LINE('',#8785,#2032);
#1688=LINE('',#8786,#2033);
#1689=LINE('',#8789,#2034);
#1690=LINE('',#8791,#2035);
#1691=LINE('',#8792,#2036);
#1692=LINE('',#8794,#2037);
#1693=LINE('',#8795,#2038);
#2015=VECTOR('',#6703,0.4);
#2016=VECTOR('',#6708,0.425);
#2017=VECTOR('',#6713,0.41);
#2018=VECTOR('',#6722,0.26);
#2019=VECTOR('',#6727,0.25);
#2020=VECTOR('',#6732,0.225);
#2021=VECTOR('',#6737,1.);
#2022=VECTOR('',#6738,1.);
#2023=VECTOR('',#6739,1.);
#2024=VECTOR('',#6740,1.);
#2025=VECTOR('',#6743,1.);
#2026=VECTOR('',#6744,1.);
#2027=VECTOR('',#6745,1.);
#2028=VECTOR('',#6748,1.);
#2029=VECTOR('',#6749,1.);
#2030=VECTOR('',#6750,1.);
#2031=VECTOR('',#6753,1.);
#2032=VECTOR('',#6754,1.);
#2033=VECTOR('',#6755,1.);
#2034=VECTOR('',#6758,1.);
#2035=VECTOR('',#6759,1.);
#2036=VECTOR('',#6760,1.);
#2037=VECTOR('',#6763,1.);
#2038=VECTOR('',#6764,1.);
#2248=CIRCLE('',#5488,0.375);
#2249=CIRCLE('',#5490,0.425);
#2250=CIRCLE('',#5492,0.425);
#2251=CIRCLE('',#5494,0.395);
#2252=CIRCLE('',#5496,0.27);
#2253=CIRCLE('',#5498,0.24505);
#2254=CIRCLE('',#5500,0.24505);
#2255=CIRCLE('',#5502,0.2);
#2589=VERTEX_POINT('',#8730);
#2590=VERTEX_POINT('',#8733);
#2591=VERTEX_POINT('',#8737);
#2592=VERTEX_POINT('',#8741);
#2593=VERTEX_POINT('',#8745);
#2594=VERTEX_POINT('',#8748);
#2595=VERTEX_POINT('',#8752);
#2596=VERTEX_POINT('',#8756);
#2597=VERTEX_POINT('',#8761);
#2598=VERTEX_POINT('',#8762);
#2599=VERTEX_POINT('',#8764);
#2600=VERTEX_POINT('',#8766);
#2601=VERTEX_POINT('',#8770);
#2602=VERTEX_POINT('',#8772);
#2603=VERTEX_POINT('',#8776);
#2604=VERTEX_POINT('',#8778);
#2605=VERTEX_POINT('',#8782);
#2606=VERTEX_POINT('',#8784);
#2607=VERTEX_POINT('',#8788);
#2608=VERTEX_POINT('',#8790);
#3123=EDGE_CURVE('',#2589,#2589,#2248,.T.);
#3124=EDGE_CURVE('',#2590,#2590,#2249,.T.);
#3125=EDGE_CURVE('',#2590,#2589,#1670,.T.);
#3126=EDGE_CURVE('',#2591,#2591,#2250,.T.);
#3127=EDGE_CURVE('',#2591,#2590,#1671,.T.);
#3128=EDGE_CURVE('',#2592,#2592,#2251,.T.);
#3129=EDGE_CURVE('',#2592,#2591,#1672,.T.);
#3130=EDGE_CURVE('',#2593,#2593,#2252,.T.);
#3131=EDGE_CURVE('',#2594,#2594,#2253,.F.);
#3132=EDGE_CURVE('',#2594,#2593,#1673,.T.);
#3133=EDGE_CURVE('',#2595,#2595,#2254,.F.);
#3134=EDGE_CURVE('',#2595,#2594,#1674,.T.);
#3135=EDGE_CURVE('',#2596,#2596,#2255,.T.);
#3136=EDGE_CURVE('',#2596,#2595,#1675,.T.);
#3137=EDGE_CURVE('',#2597,#2598,#1676,.T.);
#3138=EDGE_CURVE('',#2598,#2599,#1677,.T.);
#3139=EDGE_CURVE('',#2599,#2600,#1678,.T.);
#3140=EDGE_CURVE('',#2597,#2600,#1679,.T.);
#3141=EDGE_CURVE('',#2598,#2601,#1680,.T.);
#3142=EDGE_CURVE('',#2601,#2602,#1681,.T.);
#3143=EDGE_CURVE('',#2602,#2599,#1682,.T.);
#3144=EDGE_CURVE('',#2601,#2603,#1683,.T.);
#3145=EDGE_CURVE('',#2603,#2604,#1684,.T.);
#3146=EDGE_CURVE('',#2604,#2602,#1685,.T.);
#3147=EDGE_CURVE('',#2603,#2605,#1686,.T.);
#3148=EDGE_CURVE('',#2605,#2606,#1687,.T.);
#3149=EDGE_CURVE('',#2606,#2604,#1688,.T.);
#3150=EDGE_CURVE('',#2605,#2607,#1689,.T.);
#3151=EDGE_CURVE('',#2607,#2608,#1690,.T.);
#3152=EDGE_CURVE('',#2608,#2606,#1691,.T.);
#3153=EDGE_CURVE('',#2607,#2597,#1692,.T.);
#3154=EDGE_CURVE('',#2600,#2608,#1693,.T.);
#4159=ORIENTED_EDGE('',*,*,#3123,.F.);
#4160=ORIENTED_EDGE('',*,*,#3124,.F.);
#4161=ORIENTED_EDGE('',*,*,#3125,.T.);
#4162=ORIENTED_EDGE('',*,*,#3123,.T.);
#4163=ORIENTED_EDGE('',*,*,#3125,.F.);
#4164=ORIENTED_EDGE('',*,*,#3126,.F.);
#4165=ORIENTED_EDGE('',*,*,#3127,.T.);
#4166=ORIENTED_EDGE('',*,*,#3124,.T.);
#4167=ORIENTED_EDGE('',*,*,#3127,.F.);
#4168=ORIENTED_EDGE('',*,*,#3128,.F.);
#4169=ORIENTED_EDGE('',*,*,#3129,.T.);
#4170=ORIENTED_EDGE('',*,*,#3126,.T.);
#4171=ORIENTED_EDGE('',*,*,#3129,.F.);
#4172=ORIENTED_EDGE('',*,*,#3128,.T.);
#4173=ORIENTED_EDGE('',*,*,#3130,.F.);
#4174=ORIENTED_EDGE('',*,*,#3131,.F.);
#4175=ORIENTED_EDGE('',*,*,#3132,.T.);
#4176=ORIENTED_EDGE('',*,*,#3130,.T.);
#4177=ORIENTED_EDGE('',*,*,#3132,.F.);
#4178=ORIENTED_EDGE('',*,*,#3133,.F.);
#4179=ORIENTED_EDGE('',*,*,#3134,.T.);
#4180=ORIENTED_EDGE('',*,*,#3131,.T.);
#4181=ORIENTED_EDGE('',*,*,#3134,.F.);
#4182=ORIENTED_EDGE('',*,*,#3135,.F.);
#4183=ORIENTED_EDGE('',*,*,#3136,.T.);
#4184=ORIENTED_EDGE('',*,*,#3133,.T.);
#4185=ORIENTED_EDGE('',*,*,#3136,.F.);
#4186=ORIENTED_EDGE('',*,*,#3135,.T.);
#4187=ORIENTED_EDGE('',*,*,#3137,.T.);
#4188=ORIENTED_EDGE('',*,*,#3138,.T.);
#4189=ORIENTED_EDGE('',*,*,#3139,.T.);
#4190=ORIENTED_EDGE('',*,*,#3140,.F.);
#4191=ORIENTED_EDGE('',*,*,#3141,.T.);
#4192=ORIENTED_EDGE('',*,*,#3142,.T.);
#4193=ORIENTED_EDGE('',*,*,#3143,.T.);
#4194=ORIENTED_EDGE('',*,*,#3138,.F.);
#4195=ORIENTED_EDGE('',*,*,#3144,.T.);
#4196=ORIENTED_EDGE('',*,*,#3145,.T.);
#4197=ORIENTED_EDGE('',*,*,#3146,.T.);
#4198=ORIENTED_EDGE('',*,*,#3142,.F.);
#4199=ORIENTED_EDGE('',*,*,#3147,.T.);
#4200=ORIENTED_EDGE('',*,*,#3148,.T.);
#4201=ORIENTED_EDGE('',*,*,#3149,.T.);
#4202=ORIENTED_EDGE('',*,*,#3145,.F.);
#4203=ORIENTED_EDGE('',*,*,#3150,.T.);
#4204=ORIENTED_EDGE('',*,*,#3151,.T.);
#4205=ORIENTED_EDGE('',*,*,#3152,.T.);
#4206=ORIENTED_EDGE('',*,*,#3148,.F.);
#4207=ORIENTED_EDGE('',*,*,#3153,.T.);
#4208=ORIENTED_EDGE('',*,*,#3140,.T.);
#4209=ORIENTED_EDGE('',*,*,#3154,.T.);
#4210=ORIENTED_EDGE('',*,*,#3151,.F.);
#4211=ORIENTED_EDGE('',*,*,#3153,.F.);
#4212=ORIENTED_EDGE('',*,*,#3150,.F.);
#4213=ORIENTED_EDGE('',*,*,#3147,.F.);
#4214=ORIENTED_EDGE('',*,*,#3144,.F.);
#4215=ORIENTED_EDGE('',*,*,#3141,.F.);
#4216=ORIENTED_EDGE('',*,*,#3137,.F.);
#4217=ORIENTED_EDGE('',*,*,#3154,.F.);
#4218=ORIENTED_EDGE('',*,*,#3139,.F.);
#4219=ORIENTED_EDGE('',*,*,#3143,.F.);
#4220=ORIENTED_EDGE('',*,*,#3146,.F.);
#4221=ORIENTED_EDGE('',*,*,#3149,.F.);
#4222=ORIENTED_EDGE('',*,*,#3152,.F.);
#4472=CYLINDRICAL_SURFACE('',#5491,0.425);
#4473=CYLINDRICAL_SURFACE('',#5499,0.24505);
#4691=ADVANCED_FACE('',(#955),#703,.T.);
#4692=ADVANCED_FACE('',(#956),#26,.T.);
#4693=ADVANCED_FACE('',(#957),#4472,.T.);
#4694=ADVANCED_FACE('',(#958),#27,.T.);
#4695=ADVANCED_FACE('',(#959,#563),#704,.T.);
#4696=ADVANCED_FACE('',(#960),#28,.T.);
#4697=ADVANCED_FACE('',(#961),#4473,.T.);
#4698=ADVANCED_FACE('',(#962),#29,.T.);
#4699=ADVANCED_FACE('',(#963),#705,.T.);
#4700=ADVANCED_FACE('',(#964),#706,.F.);
#4701=ADVANCED_FACE('',(#965),#707,.F.);
#4702=ADVANCED_FACE('',(#966),#708,.F.);
#4703=ADVANCED_FACE('',(#967),#709,.F.);
#4704=ADVANCED_FACE('',(#968),#710,.F.);
#4705=ADVANCED_FACE('',(#969),#711,.F.);
#4706=ADVANCED_FACE('',(#970),#712,.F.);
#4707=ADVANCED_FACE('',(#971),#713,.F.);
#4777=CLOSED_SHELL('',(#4691,#4692,#4693,#4694,#4695,#4696,#4697,#4698,
#4699));
#4778=CLOSED_SHELL('',(#4700,#4701,#4702,#4703,#4704,#4705,#4706,#4707));
#5486=AXIS2_PLACEMENT_3D('',#8728,#6693,#6694);
#5487=AXIS2_PLACEMENT_3D('',#8729,#6695,#6696);
#5488=AXIS2_PLACEMENT_3D('',#8731,#6697,#6698);
#5489=AXIS2_PLACEMENT_3D('',#8732,#6699,#6700);
#5490=AXIS2_PLACEMENT_3D('',#8734,#6701,#6702);
#5491=AXIS2_PLACEMENT_3D('',#8736,#6704,#6705);
#5492=AXIS2_PLACEMENT_3D('',#8738,#6706,#6707);
#5493=AXIS2_PLACEMENT_3D('',#8740,#6709,#6710);
#5494=AXIS2_PLACEMENT_3D('',#8742,#6711,#6712);
#5495=AXIS2_PLACEMENT_3D('',#8744,#6714,#6715);
#5496=AXIS2_PLACEMENT_3D('',#8746,#6716,#6717);
#5497=AXIS2_PLACEMENT_3D('',#8747,#6718,#6719);
#5498=AXIS2_PLACEMENT_3D('',#8749,#6720,#6721);
#5499=AXIS2_PLACEMENT_3D('',#8751,#6723,#6724);
#5500=AXIS2_PLACEMENT_3D('',#8753,#6725,#6726);
#5501=AXIS2_PLACEMENT_3D('',#8755,#6728,#6729);
#5502=AXIS2_PLACEMENT_3D('',#8757,#6730,#6731);
#5503=AXIS2_PLACEMENT_3D('',#8759,#6733,#6734);
#5504=AXIS2_PLACEMENT_3D('',#8760,#6735,#6736);
#5505=AXIS2_PLACEMENT_3D('',#8769,#6741,#6742);
#5506=AXIS2_PLACEMENT_3D('',#8775,#6746,#6747);
#5507=AXIS2_PLACEMENT_3D('',#8781,#6751,#6752);
#5508=AXIS2_PLACEMENT_3D('',#8787,#6756,#6757);
#5509=AXIS2_PLACEMENT_3D('',#8793,#6761,#6762);
#5510=AXIS2_PLACEMENT_3D('',#8796,#6765,#6766);
#5511=AXIS2_PLACEMENT_3D('',#8797,#6767,#6768);
#6693=DIRECTION('axis',(0.,0.,1.));
#6694=DIRECTION('refdir',(1.,0.,0.));
#6695=DIRECTION('center_axis',(0.,1.,0.));
#6696=DIRECTION('ref_axis',(0.,0.,1.));
#6697=DIRECTION('center_axis',(0.,-1.,0.));
#6698=DIRECTION('ref_axis',(1.,0.,0.));
#6699=DIRECTION('center_axis',(0.,-1.,0.));
#6700=DIRECTION('ref_axis',(1.,0.,0.));
#6701=DIRECTION('center_axis',(0.,-1.,0.));
#6702=DIRECTION('ref_axis',(1.,0.,0.));
#6703=DIRECTION('',(0.707106781186548,0.707106781186547,8.65956056235493E-17));
#6704=DIRECTION('center_axis',(0.,-1.,0.));
#6705=DIRECTION('ref_axis',(1.,0.,0.));
#6706=DIRECTION('center_axis',(0.,-1.,0.));
#6707=DIRECTION('ref_axis',(1.,0.,0.));
#6708=DIRECTION('',(0.,1.,0.));
#6709=DIRECTION('center_axis',(0.,1.,0.));
#6710=DIRECTION('ref_axis',(1.,0.,0.));
#6711=DIRECTION('center_axis',(0.,-1.,0.));
#6712=DIRECTION('ref_axis',(1.,0.,0.));
#6713=DIRECTION('',(-0.707106781186547,0.707106781186548,-8.65956056235493E-17));
#6714=DIRECTION('center_axis',(0.,-1.,0.));
#6715=DIRECTION('ref_axis',(0.,0.,-1.));
#6716=DIRECTION('center_axis',(0.,-1.,0.));
#6717=DIRECTION('ref_axis',(1.,0.,0.));
#6718=DIRECTION('center_axis',(0.,1.,0.));
#6719=DIRECTION('ref_axis',(1.,0.,0.));
#6720=DIRECTION('center_axis',(0.,1.,0.));
#6721=DIRECTION('ref_axis',(1.,0.,0.));
#6722=DIRECTION('',(-0.447213595499958,0.894427190999916,-5.47678698264203E-17));
#6723=DIRECTION('center_axis',(0.,-1.,0.));
#6724=DIRECTION('ref_axis',(1.,0.,0.));
#6725=DIRECTION('center_axis',(0.,1.,0.));
#6726=DIRECTION('ref_axis',(1.,0.,0.));
#6727=DIRECTION('',(0.,1.,0.));
#6728=DIRECTION('center_axis',(0.,1.,0.));
#6729=DIRECTION('ref_axis',(1.,0.,0.));
#6730=DIRECTION('center_axis',(0.,-1.,0.));
#6731=DIRECTION('ref_axis',(1.,0.,0.));
#6732=DIRECTION('',(-0.707106781186547,0.707106781186548,-8.65956056235493E-17));
#6733=DIRECTION('center_axis',(0.,-1.,0.));
#6734=DIRECTION('ref_axis',(0.,0.,-1.));
#6735=DIRECTION('center_axis',(0.866025403784439,0.,-0.5));
#6736=DIRECTION('ref_axis',(0.5,0.,0.866025403784439));
#6737=DIRECTION('',(-0.5,0.,-0.866025403784439));
#6738=DIRECTION('',(0.,-1.,0.));
#6739=DIRECTION('',(0.5,0.,0.866025403784439));
#6740=DIRECTION('',(0.,-1.,0.));
#6741=DIRECTION('center_axis',(1.20185167898973E-16,0.,-1.));
#6742=DIRECTION('ref_axis',(1.,0.,1.20185167898973E-16));
#6743=DIRECTION('',(-1.,0.,-1.20185167898973E-16));
#6744=DIRECTION('',(0.,-1.,0.));
#6745=DIRECTION('',(1.,0.,1.20185167898973E-16));
#6746=DIRECTION('center_axis',(-0.866025403784439,0.,-0.5));
#6747=DIRECTION('ref_axis',(0.5,0.,-0.866025403784439));
#6748=DIRECTION('',(-0.5,0.,0.866025403784439));
#6749=DIRECTION('',(0.,-1.,0.));
#6750=DIRECTION('',(0.5,0.,-0.866025403784439));
#6751=DIRECTION('center_axis',(-0.866025403784439,0.,0.5));
#6752=DIRECTION('ref_axis',(-0.5,0.,-0.866025403784439));
#6753=DIRECTION('',(0.5,0.,0.866025403784439));
#6754=DIRECTION('',(0.,-1.,0.));
#6755=DIRECTION('',(-0.5,0.,-0.866025403784439));
#6756=DIRECTION('center_axis',(-2.40370335797945E-16,0.,1.));
#6757=DIRECTION('ref_axis',(-1.,0.,-2.40370335797945E-16));
#6758=DIRECTION('',(1.,0.,2.40370335797945E-16));
#6759=DIRECTION('',(0.,-1.,0.));
#6760=DIRECTION('',(-1.,0.,-2.40370335797945E-16));
#6761=DIRECTION('center_axis',(0.866025403784439,0.,0.5));
#6762=DIRECTION('ref_axis',(-0.5,0.,0.866025403784439));
#6763=DIRECTION('',(0.5,0.,-0.866025403784439));
#6764=DIRECTION('',(-0.5,0.,0.866025403784439));
#6765=DIRECTION('center_axis',(0.,1.,0.));
#6766=DIRECTION('ref_axis',(1.,0.,0.));
#6767=DIRECTION('center_axis',(0.,-1.,0.));
#6768=DIRECTION('ref_axis',(0.,0.,-1.));
#8728=CARTESIAN_POINT('',(0.,0.,0.));
#8729=CARTESIAN_POINT('Origin',(0.375,0.5,0.));
#8730=CARTESIAN_POINT('',(-0.375,0.5,-4.59242549680257E-17));
#8731=CARTESIAN_POINT('Origin',(0.,0.5,0.));
#8732=CARTESIAN_POINT('Origin',(0.,0.475,0.));
#8733=CARTESIAN_POINT('',(-0.425,0.45,-5.20474889637625E-17));
#8734=CARTESIAN_POINT('Origin',(0.,0.45,0.));
#8735=CARTESIAN_POINT('',(-0.4,0.475,-4.89858719658941E-17));
#8736=CARTESIAN_POINT('Origin',(0.,0.24,0.));
#8737=CARTESIAN_POINT('',(-0.425,0.0299999999999998,-5.20474889637625E-17));
#8738=CARTESIAN_POINT('Origin',(0.,0.0299999999999998,0.));
#8739=CARTESIAN_POINT('',(-0.425,0.24,-5.20474889637625E-17));
#8740=CARTESIAN_POINT('Origin',(0.,0.0150000000000001,0.));
#8741=CARTESIAN_POINT('',(-0.395,4.85722573273506E-17,-4.83735485663204E-17));
#8742=CARTESIAN_POINT('Origin',(0.,0.,0.));
#8743=CARTESIAN_POINT('',(-0.41,0.0150000000000001,-5.02105187650415E-17));
#8744=CARTESIAN_POINT('Origin',(0.27,0.,0.));
#8745=CARTESIAN_POINT('',(-0.27,0.,-3.30654635769785E-17));
#8746=CARTESIAN_POINT('Origin',(0.,0.,0.));
#8747=CARTESIAN_POINT('Origin',(0.,-0.02,0.));
#8748=CARTESIAN_POINT('',(-0.24505,-0.0498999999999999,3.00099698131059E-17));
#8749=CARTESIAN_POINT('Origin',(0.,-0.0498999999999999,0.));
#8750=CARTESIAN_POINT('',(-0.26,-0.02,-3.18408167778312E-17));
#8751=CARTESIAN_POINT('Origin',(0.,-0.995,0.));
#8752=CARTESIAN_POINT('',(-0.24505,-1.95495,3.00099698131059E-17));
#8753=CARTESIAN_POINT('Origin',(0.,-1.95495,0.));
#8754=CARTESIAN_POINT('',(-0.24505,-0.995,-3.00099698131059E-17));
#8755=CARTESIAN_POINT('Origin',(0.,-1.975,0.));
#8756=CARTESIAN_POINT('',(-0.2,-2.,-2.44929359829471E-17));
#8757=CARTESIAN_POINT('Origin',(0.,-2.,0.));
#8758=CARTESIAN_POINT('',(-0.225,-1.975,-2.75545529808154E-17));
#8759=CARTESIAN_POINT('Origin',(0.,-2.,0.));
#8760=CARTESIAN_POINT('Origin',(0.115470053837925,-0.5,-0.2));
#8761=CARTESIAN_POINT('',(0.23094010767585,-0.5,0.));
#8762=CARTESIAN_POINT('',(0.115470053837925,-0.5,-0.2));
#8763=CARTESIAN_POINT('',(0.23094010767585,-0.5,0.));
#8764=CARTESIAN_POINT('',(0.115470053837925,-0.8,-0.2));
#8765=CARTESIAN_POINT('',(0.115470053837925,-0.5,-0.2));
#8766=CARTESIAN_POINT('',(0.23094010767585,-0.8,0.));
#8767=CARTESIAN_POINT('',(0.23094010767585,-0.8,0.));
#8768=CARTESIAN_POINT('',(0.23094010767585,-0.5,0.));
#8769=CARTESIAN_POINT('Origin',(-0.115470053837925,-0.5,-0.2));
#8770=CARTESIAN_POINT('',(-0.115470053837925,-0.5,-0.2));
#8771=CARTESIAN_POINT('',(0.115470053837925,-0.5,-0.2));
#8772=CARTESIAN_POINT('',(-0.115470053837925,-0.8,-0.2));
#8773=CARTESIAN_POINT('',(-0.115470053837925,-0.5,-0.2));
#8774=CARTESIAN_POINT('',(0.115470053837925,-0.8,-0.2));
#8775=CARTESIAN_POINT('Origin',(-0.23094010767585,-0.5,-2.77555756156289E-17));
#8776=CARTESIAN_POINT('',(-0.23094010767585,-0.5,-2.82820063659975E-17));
#8777=CARTESIAN_POINT('',(-0.115470053837925,-0.5,-0.2));
#8778=CARTESIAN_POINT('',(-0.23094010767585,-0.8,-2.77555756156289E-17));
#8779=CARTESIAN_POINT('',(-0.23094010767585,-0.5,-2.82820063659975E-17));
#8780=CARTESIAN_POINT('',(-0.115470053837925,-0.8,-0.2));
#8781=CARTESIAN_POINT('Origin',(-0.115470053837925,-0.5,0.2));
#8782=CARTESIAN_POINT('',(-0.115470053837925,-0.5,0.2));
#8783=CARTESIAN_POINT('',(-0.23094010767585,-0.5,-2.82820063659975E-17));
#8784=CARTESIAN_POINT('',(-0.115470053837925,-0.8,0.2));
#8785=CARTESIAN_POINT('',(-0.115470053837925,-0.5,0.2));
#8786=CARTESIAN_POINT('',(-0.23094010767585,-0.8,-2.82820063659975E-17));
#8787=CARTESIAN_POINT('Origin',(0.115470053837925,-0.5,0.2));
#8788=CARTESIAN_POINT('',(0.115470053837925,-0.5,0.2));
#8789=CARTESIAN_POINT('',(-0.115470053837925,-0.5,0.2));
#8790=CARTESIAN_POINT('',(0.115470053837925,-0.8,0.2));
#8791=CARTESIAN_POINT('',(0.115470053837925,-0.5,0.2));
#8792=CARTESIAN_POINT('',(-0.115470053837925,-0.8,0.2));
#8793=CARTESIAN_POINT('Origin',(0.23094010767585,-0.5,0.));
#8794=CARTESIAN_POINT('',(0.115470053837925,-0.5,0.2));
#8795=CARTESIAN_POINT('',(0.115470053837925,-0.8,0.2));
#8796=CARTESIAN_POINT('Origin',(0.,-0.5,0.));
#8797=CARTESIAN_POINT('Origin',(0.,-0.8,0.));
#9103=UNCERTAINTY_MEASURE_WITH_UNIT(LENGTH_MEASURE(0.001),#9142,
'DISTANCE_ACCURACY_VALUE',
'Maximum model space distance between geometric entities at asserted c
onnectivities');
#9108=UNCERTAINTY_MEASURE_WITH_UNIT(LENGTH_MEASURE(0.001),#9142,
'DISTANCE_ACCURACY_VALUE',
'Maximum model space distance between geometric entities at asserted c
onnectivities');
#9136=(
GEOMETRIC_REPRESENTATION_CONTEXT(3)
GLOBAL_UNCERTAINTY_ASSIGNED_CONTEXT((#9103))
GLOBAL_UNIT_ASSIGNED_CONTEXT((#9142,#9144,#9145))
REPRESENTATION_CONTEXT('','3D')
);
#9141=(
GEOMETRIC_REPRESENTATION_CONTEXT(3)
GLOBAL_UNCERTAINTY_ASSIGNED_CONTEXT((#9108))
GLOBAL_UNIT_ASSIGNED_CONTEXT((#9142,#9144,#9145))
REPRESENTATION_CONTEXT('','3D')
);
#9142=(
LENGTH_UNIT()
NAMED_UNIT(*)
SI_UNIT(.CENTI.,.METRE.)
);
#9144=(
NAMED_UNIT(*)
PLANE_ANGLE_UNIT()
SI_UNIT($,.RADIAN.)
);
#9145=(
NAMED_UNIT(*)
SI_UNIT($,.STERADIAN.)
SOLID_ANGLE_UNIT()
);
#9173=SHAPE_DEFINITION_REPRESENTATION(#9207,#9301);
#9207=PRODUCT_DEFINITION_SHAPE('',$,#9334);
#9301=SHAPE_REPRESENTATION('',(#5486),#9136);
#9306=PRODUCT_DEFINITION_CONTEXT('part definition',#9404,'design');
#9334=PRODUCT_DEFINITION('Cap Screw - M5x20','Cap Screw - M5x20',#9366,
#9306);
#9366=PRODUCT_DEFINITION_FORMATION('',$,#9433);
#9404=APPLICATION_CONTEXT(
'Core Data for Automotive Mechanical Design Process');
#9405=PRODUCT_CONTEXT('part definition',#9404,'mechanical');
#9433=PRODUCT('Cap Screw - M5x20','Cap Screw - M5x20',
'Cap Screw - M5x20',(#9405));
#9501=COLOUR_RGB('Black',0.12,0.14,0.17);
#9502=FILL_AREA_STYLE_COLOUR('',#9501);
#9503=FILL_AREA_STYLE('',(#9502));
#9504=SURFACE_STYLE_FILL_AREA(#9503);
#9505=SURFACE_SIDE_STYLE('',(#9504));
#9506=SURFACE_STYLE_USAGE(.BOTH.,#9505);
#9507=PRESENTATION_STYLE_ASSIGNMENT((#9506));
ENDSEC;
END-ISO-10303-21;
